ISO-10303-21;
HEADER;
/* Generated by software containing ST-Developer
 * from STEP Tools, Inc. (www.steptools.com) 
 */

FILE_DESCRIPTION(
/* description */ ('Bin tilter linkage'),
/* implementation_level */ '2;1');

FILE_NAME(
/* name */ 'M4 short cap screw (10).step',
/* time_stamp */ '2026-10-28T03:26:24-07:00',
/* author */ (''),
/* organization */ (''),
/* preprocessor_version */ 'ST-DEVELOPER v20.2',
/* originating_system */ 'Autodesk Translation Framework v15.17.0.0',
/* authorisation */ '');

FILE_SCHEMA (('AUTOMOTIVE_DESIGN { 1 0 10303 214 3 1 1 }'));
ENDSEC;

DATA;
#10=MECHANICAL_DESIGN_GEOMETRIC_PRESENTATION_REPRESENTATION('',(#906),#23728);
#694=SHAPE_REPRESENTATION_RELATIONSHIP('SRR','None',#24159,#800);
#800=ADVANCED_BREP_SHAPE_REPRESENTATION('',(#1019),#23659);
#906=STYLED_ITEM('',(#24772),#1019);
#1019=MANIFOLD_SOLID_BREP('Body1',#12437);
#1294=FACE_BOUND('',#3214,.T.);
#1657=PLANE('',#14407);
#1658=PLANE('',#14412);
#1659=PLANE('',#14415);
#2229=FACE_OUTER_BOUND('',#3213,.T.);
#2230=FACE_OUTER_BOUND('',#3215,.T.);
#2231=FACE_OUTER_BOUND('',#3216,.T.);
#2232=FACE_OUTER_BOUND('',#3217,.T.);
#2233=FACE_OUTER_BOUND('',#3218,.T.);
#3213=EDGE_LOOP('',(#9685));
#3214=EDGE_LOOP('',(#9686));
#3215=EDGE_LOOP('',(#9687,#9688,#9689,#9690));
#3216=EDGE_LOOP('',(#9691));
#3217=EDGE_LOOP('',(#9692,#9693,#9694,#9695));
#3218=EDGE_LOOP('',(#9696));
#4161=LINE('',#21231,#4836);
#4162=LINE('',#21237,#4837);
#4836=VECTOR('',#17256,0.35);
#4837=VECTOR('',#17265,0.199999999999999);
#5543=CIRCLE('',#14408,0.35);
#5544=CIRCLE('',#14409,0.199999999999999);
#5545=CIRCLE('',#14411,0.35);
#5546=CIRCLE('',#14414,0.199999999999999);
#6393=VERTEX_POINT('',#21225);
#6394=VERTEX_POINT('',#21227);
#6395=VERTEX_POINT('',#21230);
#6396=VERTEX_POINT('',#21235);
#7582=EDGE_CURVE('',#6393,#6393,#5543,.T.);
#7583=EDGE_CURVE('',#6394,#6394,#5544,.T.);
#7584=EDGE_CURVE('',#6393,#6395,#4161,.T.);
#7585=EDGE_CURVE('',#6395,#6395,#5545,.T.);
#7586=EDGE_CURVE('',#6396,#6396,#5546,.T.);
#7587=EDGE_CURVE('',#6396,#6394,#4162,.T.);
#9685=ORIENTED_EDGE('',*,*,#7582,.T.);
#9686=ORIENTED_EDGE('',*,*,#7583,.F.);
#9687=ORIENTED_EDGE('',*,*,#7582,.F.);
#9688=ORIENTED_EDGE('',*,*,#7584,.T.);
#9689=ORIENTED_EDGE('',*,*,#7585,.T.);
#9690=ORIENTED_EDGE('',*,*,#7584,.F.);
#9691=ORIENTED_EDGE('',*,*,#7585,.F.);
#9692=ORIENTED_EDGE('',*,*,#7586,.F.);
#9693=ORIENTED_EDGE('',*,*,#7587,.T.);
#9694=ORIENTED_EDGE('',*,*,#7583,.T.);
#9695=ORIENTED_EDGE('',*,*,#7587,.F.);
#9696=ORIENTED_EDGE('',*,*,#7586,.T.);
#11437=CYLINDRICAL_SURFACE('',#14410,0.35);
#11438=CYLINDRICAL_SURFACE('',#14413,0.199999999999999);
#11954=ADVANCED_FACE('',(#2229,#1294),#1657,.T.);
#11955=ADVANCED_FACE('',(#2230),#11437,.T.);
#11956=ADVANCED_FACE('',(#2231),#1658,.F.);
#11957=ADVANCED_FACE('',(#2232),#11438,.T.);
#11958=ADVANCED_FACE('',(#2233),#1659,.T.);
#12437=CLOSED_SHELL('',(#11954,#11955,#11956,#11957,#11958));
#14406=AXIS2_PLACEMENT_3D('',#21223,#17246,#17247);
#14407=AXIS2_PLACEMENT_3D('',#21224,#17248,#17249);
#14408=AXIS2_PLACEMENT_3D('',#21226,#17250,#17251);
#14409=AXIS2_PLACEMENT_3D('',#21228,#17252,#17253);
#14410=AXIS2_PLACEMENT_3D('',#21229,#17254,#17255);
#14411=AXIS2_PLACEMENT_3D('',#21232,#17257,#17258);
#14412=AXIS2_PLACEMENT_3D('',#21233,#17259,#17260);
#14413=AXIS2_PLACEMENT_3D('',#21234,#17261,#17262);
#14414=AXIS2_PLACEMENT_3D('',#21236,#17263,#17264);
#14415=AXIS2_PLACEMENT_3D('',#21238,#17266,#17267);
#17246=DIRECTION('axis',(0.,0.,1.));
#17247=DIRECTION('refdir',(1.,0.,0.));
#17248=DIRECTION('center_axis',(0.,1.,0.));
#17249=DIRECTION('ref_axis',(1.,0.,0.));
#17250=DIRECTION('center_axis',(0.,1.,0.));
#17251=DIRECTION('ref_axis',(1.,0.,0.));
#17252=DIRECTION('center_axis',(0.,1.,0.));
#17253=DIRECTION('ref_axis',(1.,0.,0.));
#17254=DIRECTION('center_axis',(0.,1.,0.));
#17255=DIRECTION('ref_axis',(1.,0.,0.));
#17256=DIRECTION('',(0.,-1.,0.));
#17257=DIRECTION('center_axis',(0.,1.,0.));
#17258=DIRECTION('ref_axis',(1.,0.,0.));
#17259=DIRECTION('center_axis',(0.,1.,0.));
#17260=DIRECTION('ref_axis',(1.,0.,0.));
#17261=DIRECTION('center_axis',(0.,1.,0.));
#17262=DIRECTION('ref_axis',(1.,0.,0.));
#17263=DIRECTION('center_axis',(0.,1.,0.));
#17264=DIRECTION('ref_axis',(1.,0.,0.));
#17265=DIRECTION('',(0.,-1.,0.));
#17266=DIRECTION('center_axis',(0.,1.,0.));
#17267=DIRECTION('ref_axis',(1.,0.,0.));
#21223=CARTESIAN_POINT('',(0.,0.,0.));
#21224=CARTESIAN_POINT('Origin',(8.08877866266397,-0.8,17.1120538880616));
#21225=CARTESIAN_POINT('',(7.73877866266397,-0.8,17.1120538880616));
#21226=CARTESIAN_POINT('Origin',(8.08877866266397,-0.8,17.1120538880616));
#21227=CARTESIAN_POINT('',(7.88877866266397,-0.8,17.1120538880616));
#21228=CARTESIAN_POINT('Origin',(8.08877866266397,-0.8,17.1120538880616));
#21229=CARTESIAN_POINT('Origin',(8.08877866266397,-1.2,17.1120538880616));
#21230=CARTESIAN_POINT('',(7.73877866266397,-1.2,17.1120538880616));
#21231=CARTESIAN_POINT('',(7.73877866266397,-1.2,17.1120538880616));
#21232=CARTESIAN_POINT('Origin',(8.08877866266397,-1.2,17.1120538880616));
#21233=CARTESIAN_POINT('Origin',(8.08877866266397,-1.2,17.1120538880616));
#21234=CARTESIAN_POINT('Origin',(8.08877866266397,-0.8,17.1120538880616));
#21235=CARTESIAN_POINT('',(7.88877866266397,-0.1,17.1120538880616));
#21236=CARTESIAN_POINT('Origin',(8.08877866266397,-0.1,17.1120538880616));
#21237=CARTESIAN_POINT('',(7.88877866266397,-0.8,17.1120538880616));
#21238=CARTESIAN_POINT('Origin',(8.08877866266397,-0.1,17.1120538880616));
#23542=UNCERTAINTY_MEASURE_WITH_UNIT(LENGTH_MEASURE(0.001),#23729,
'DISTANCE_ACCURACY_VALUE',
'Maximum model space distance between geometric entities at asserted c
onnectivities');
#23611=UNCERTAINTY_MEASURE_WITH_UNIT(LENGTH_MEASURE(0.001),#23729,
'DISTANCE_ACCURACY_VALUE',
'Maximum model space distance between geometric entities at asserted c
onnectivities');
#23659=(
GEOMETRIC_REPRESENTATION_CONTEXT(3)
GLOBAL_UNCERTAINTY_ASSIGNED_CONTEXT((#23542))
GLOBAL_UNIT_ASSIGNED_CONTEXT((#23729,#23731,#23732))
REPRESENTATION_CONTEXT('','3D')
);
#23728=(
GEOMETRIC_REPRESENTATION_CONTEXT(3)
GLOBAL_UNCERTAINTY_ASSIGNED_CONTEXT((#23611))
GLOBAL_UNIT_ASSIGNED_CONTEXT((#23729,#23731,#23732))
REPRESENTATION_CONTEXT('','3D')
);
#23729=(
LENGTH_UNIT()
NAMED_UNIT(*)
SI_UNIT(.CENTI.,.METRE.)
);
#23731=(
NAMED_UNIT(*)
PLANE_ANGLE_UNIT()
SI_UNIT($,.RADIAN.)
);
#23732=(
NAMED_UNIT(*)
SI_UNIT($,.STERADIAN.)
SOLID_ANGLE_UNIT()
);
#23780=SHAPE_DEFINITION_REPRESENTATION(#23896,#24159);
#23896=PRODUCT_DEFINITION_SHAPE('',$,#24276);
#24159=SHAPE_REPRESENTATION('',(#14406),#23659);
#24228=PRODUCT_DEFINITION_CONTEXT('part definition',#24578,'design');
#24276=PRODUCT_DEFINITION('M4 short cap screw (10)',
'M4 short cap screw (10)',#24392,#24228);
#24392=PRODUCT_DEFINITION_FORMATION('',$,#24627);
#24578=APPLICATION_CONTEXT(
'Core Data for Automotive Mechanical Design Process');
#24579=PRODUCT_CONTEXT('part definition',#24578,'mechanical');
#24627=PRODUCT('M4 short cap screw (10)','M4 short cap screw (10)',
'M4 short cap screw (10)',(#24579));
#24766=COLOUR_RGB('Black',0.12,0.14,0.17);
#24767=FILL_AREA_STYLE_COLOUR('',#24766);
#24768=FILL_AREA_STYLE('',(#24767));
#24769=SURFACE_STYLE_FILL_AREA(#24768);
#24770=SURFACE_SIDE_STYLE('',(#24769));
#24771=SURFACE_STYLE_USAGE(.BOTH.,#24770);
#24772=PRESENTATION_STYLE_ASSIGNMENT((#24771));
ENDSEC;
END-ISO-10303-21;
